ISO-10303-21;
HEADER;
/* Generated by software containing ST-Developer
 * from STEP Tools, Inc. (www.steptools.com) 
 */

FILE_DESCRIPTION(
/* description */ ('PAT-091'),
/* implementation_level */ '2;1');

FILE_NAME(
/* name */ 'Axle distance sleeve 5 mm (4).step',
/* time_stamp */ '2026-10-27T15:34:44-07:00',
/* author */ (''),
/* organization */ (''),
/* preprocessor_version */ 'ST-DEVELOPER v20.2',
/* originating_system */ 'Autodesk Translation Framework v15.17.0.0',
/* authorisation */ '');

FILE_SCHEMA (('AUTOMOTIVE_DESIGN { 1 0 10303 214 3 1 1 }'));
ENDSEC;

DATA;
#10=MECHANICAL_DESIGN_GEOMETRIC_PRESENTATION_REPRESENTATION('',(#1000),#25100);
#780=SHAPE_REPRESENTATION_RELATIONSHIP('SRR','None',#25542,#890);
#890=ADVANCED_BREP_SHAPE_REPRESENTATION('',(#1123),#25012);
#1000=STYLED_ITEM('',(#26191),#1123);
#1123=MANIFOLD_SOLID_BREP('Body1',#13278);
#1389=FACE_BOUND('',#3297,.T.);
#1390=FACE_BOUND('',#3299,.T.);
#1764=PLANE('',#15090);
#1765=PLANE('',#15091);
#2302=FACE_OUTER_BOUND('',#3294,.T.);
#2303=FACE_OUTER_BOUND('',#3295,.T.);
#2304=FACE_OUTER_BOUND('',#3296,.T.);
#2305=FACE_OUTER_BOUND('',#3298,.T.);
#3294=EDGE_LOOP('',(#9980,#9981,#9982,#9983));
#3295=EDGE_LOOP('',(#9984,#9985,#9986,#9987));
#3296=EDGE_LOOP('',(#9988));
#3297=EDGE_LOOP('',(#9989));
#3298=EDGE_LOOP('',(#9990));
#3299=EDGE_LOOP('',(#9991));
#4401=LINE('',#22089,#5141);
#4402=LINE('',#22095,#5142);
#5141=VECTOR('',#17747,0.605);
#5142=VECTOR('',#17754,0.8);
#5831=CIRCLE('',#15085,0.605);
#5832=CIRCLE('',#15086,0.605);
#5833=CIRCLE('',#15088,0.8);
#5834=CIRCLE('',#15089,0.8);
#6718=VERTEX_POINT('',#22086);
#6719=VERTEX_POINT('',#22088);
#6720=VERTEX_POINT('',#22092);
#6721=VERTEX_POINT('',#22094);
#7925=EDGE_CURVE('',#6718,#6718,#5831,.T.);
#7926=EDGE_CURVE('',#6718,#6719,#4401,.T.);
#7927=EDGE_CURVE('',#6719,#6719,#5832,.T.);
#7928=EDGE_CURVE('',#6720,#6720,#5833,.T.);
#7929=EDGE_CURVE('',#6720,#6721,#4402,.T.);
#7930=EDGE_CURVE('',#6721,#6721,#5834,.T.);
#9980=ORIENTED_EDGE('',*,*,#7925,.F.);
#9981=ORIENTED_EDGE('',*,*,#7926,.T.);
#9982=ORIENTED_EDGE('',*,*,#7927,.T.);
#9983=ORIENTED_EDGE('',*,*,#7926,.F.);
#9984=ORIENTED_EDGE('',*,*,#7928,.F.);
#9985=ORIENTED_EDGE('',*,*,#7929,.T.);
#9986=ORIENTED_EDGE('',*,*,#7930,.T.);
#9987=ORIENTED_EDGE('',*,*,#7929,.F.);
#9988=ORIENTED_EDGE('',*,*,#7928,.T.);
#9989=ORIENTED_EDGE('',*,*,#7925,.T.);
#9990=ORIENTED_EDGE('',*,*,#7930,.F.);
#9991=ORIENTED_EDGE('',*,*,#7927,.F.);
#12186=CYLINDRICAL_SURFACE('',#15084,0.605);
#12187=CYLINDRICAL_SURFACE('',#15087,0.8);
#12669=ADVANCED_FACE('',(#2302),#12186,.F.);
#12670=ADVANCED_FACE('',(#2303),#12187,.T.);
#12671=ADVANCED_FACE('',(#2304,#1389),#1764,.T.);
#12672=ADVANCED_FACE('',(#2305,#1390),#1765,.F.);
#13278=CLOSED_SHELL('',(#12669,#12670,#12671,#12672));
#15083=AXIS2_PLACEMENT_3D('',#22084,#17741,#17742);
#15084=AXIS2_PLACEMENT_3D('',#22085,#17743,#17744);
#15085=AXIS2_PLACEMENT_3D('',#22087,#17745,#17746);
#15086=AXIS2_PLACEMENT_3D('',#22090,#17748,#17749);
#15087=AXIS2_PLACEMENT_3D('',#22091,#17750,#17751);
#15088=AXIS2_PLACEMENT_3D('',#22093,#17752,#17753);
#15089=AXIS2_PLACEMENT_3D('',#22096,#17755,#17756);
#15090=AXIS2_PLACEMENT_3D('',#22097,#17757,#17758);
#15091=AXIS2_PLACEMENT_3D('',#22098,#17759,#17760);
#17741=DIRECTION('axis',(0.,0.,1.));
#17742=DIRECTION('refdir',(1.,0.,0.));
#17743=DIRECTION('center_axis',(0.,1.,0.));
#17744=DIRECTION('ref_axis',(1.,0.,0.));
#17745=DIRECTION('center_axis',(0.,-1.,0.));
#17746=DIRECTION('ref_axis',(1.,0.,0.));
#17747=DIRECTION('',(0.,-1.,0.));
#17748=DIRECTION('center_axis',(0.,-1.,0.));
#17749=DIRECTION('ref_axis',(1.,0.,0.));
#17750=DIRECTION('center_axis',(0.,1.,0.));
#17751=DIRECTION('ref_axis',(1.,0.,0.));
#17752=DIRECTION('center_axis',(0.,1.,0.));
#17753=DIRECTION('ref_axis',(1.,0.,0.));
#17754=DIRECTION('',(0.,-1.,0.));
#17755=DIRECTION('center_axis',(0.,1.,0.));
#17756=DIRECTION('ref_axis',(1.,0.,0.));
#17757=DIRECTION('center_axis',(0.,1.,0.));
#17758=DIRECTION('ref_axis',(1.,0.,0.));
#17759=DIRECTION('center_axis',(0.,1.,0.));
#17760=DIRECTION('ref_axis',(1.,0.,0.));
#22084=CARTESIAN_POINT('',(0.,0.,0.));
#22085=CARTESIAN_POINT('Origin',(0.,8.,13.));
#22086=CARTESIAN_POINT('',(-0.605,8.5,13.));
#22087=CARTESIAN_POINT('Origin',(0.,8.5,13.));
#22088=CARTESIAN_POINT('',(-0.605,8.,13.));
#22089=CARTESIAN_POINT('',(-0.605,8.,13.));
#22090=CARTESIAN_POINT('Origin',(0.,8.,13.));
#22091=CARTESIAN_POINT('Origin',(0.,8.,13.));
#22092=CARTESIAN_POINT('',(-0.8,8.5,13.));
#22093=CARTESIAN_POINT('Origin',(0.,8.5,13.));
#22094=CARTESIAN_POINT('',(-0.8,8.,13.));
#22095=CARTESIAN_POINT('',(-0.8,8.,13.));
#22096=CARTESIAN_POINT('Origin',(0.,8.,13.));
#22097=CARTESIAN_POINT('Origin',(0.,8.5,13.));
#22098=CARTESIAN_POINT('Origin',(0.,8.,13.));
#24891=UNCERTAINTY_MEASURE_WITH_UNIT(LENGTH_MEASURE(0.001),#25101,
'DISTANCE_ACCURACY_VALUE',
'Maximum model space distance between geometric entities at asserted c
onnectivities');
#24979=UNCERTAINTY_MEASURE_WITH_UNIT(LENGTH_MEASURE(0.001),#25101,
'DISTANCE_ACCURACY_VALUE',
'Maximum model space distance between geometric entities at asserted c
onnectivities');
#25012=(
GEOMETRIC_REPRESENTATION_CONTEXT(3)
GLOBAL_UNCERTAINTY_ASSIGNED_CONTEXT((#24891))
GLOBAL_UNIT_ASSIGNED_CONTEXT((#25101,#25103,#25104))
REPRESENTATION_CONTEXT('','3D')
);
#25100=(
GEOMETRIC_REPRESENTATION_CONTEXT(3)
GLOBAL_UNCERTAINTY_ASSIGNED_CONTEXT((#24979))
GLOBAL_UNIT_ASSIGNED_CONTEXT((#25101,#25103,#25104))
REPRESENTATION_CONTEXT('','3D')
);
#25101=(
LENGTH_UNIT()
NAMED_UNIT(*)
SI_UNIT(.CENTI.,.METRE.)
);
#25103=(
NAMED_UNIT(*)
PLANE_ANGLE_UNIT()
SI_UNIT($,.RADIAN.)
);
#25104=(
NAMED_UNIT(*)
SI_UNIT($,.STERADIAN.)
SOLID_ANGLE_UNIT()
);
#25137=SHAPE_DEFINITION_REPRESENTATION(#25257,#25542);
#25257=PRODUCT_DEFINITION_SHAPE('',$,#25663);
#25542=SHAPE_REPRESENTATION('',(#15083),#25012);
#25630=PRODUCT_DEFINITION_CONTEXT('part definition',#25992,'design');
#25663=PRODUCT_DEFINITION('Axle distance sleeve 5 mm (4)',
'Axle distance sleeve 5 mm (4)',#25783,#25630);
#25783=PRODUCT_DEFINITION_FORMATION('',$,#26026);
#25992=APPLICATION_CONTEXT(
'Core Data for Automotive Mechanical Design Process');
#25993=PRODUCT_CONTEXT('part definition',#25992,'mechanical');
#26026=PRODUCT('Axle distance sleeve 5 mm (4)',
'Axle distance sleeve 5 mm (4)','Axle distance sleeve 5 mm (4)',(#25993));
#26185=COLOUR_RGB('Grey',0.48,0.52,0.57);
#26186=FILL_AREA_STYLE_COLOUR('',#26185);
#26187=FILL_AREA_STYLE('',(#26186));
#26188=SURFACE_STYLE_FILL_AREA(#26187);
#26189=SURFACE_SIDE_STYLE('',(#26188));
#26190=SURFACE_STYLE_USAGE(.BOTH.,#26189);
#26191=PRESENTATION_STYLE_ASSIGNMENT((#26190));
ENDSEC;
END-ISO-10303-21;
